ISO-10303-21;
HEADER;
/* Generated by software containing ST-Developer
 * from STEP Tools, Inc. (www.steptools.com) 
 */

FILE_DESCRIPTION(
/* description */ (''),
/* implementation_level */ '2;1');

FILE_NAME(
/* name */ 'Screw.step',
/* time_stamp */ '2026-10-12T16:07:47-07:00',
/* author */ (''),
/* organization */ (''),
/* preprocessor_version */ 'ST-DEVELOPER v20.2',
/* originating_system */ 'Autodesk Translation Framework v15.15.0.0',
/* authorisation */ '');

FILE_SCHEMA (('AUTOMOTIVE_DESIGN { 1 0 10303 214 3 1 1 }'));
ENDSEC;

DATA;
#10=MECHANICAL_DESIGN_GEOMETRIC_PRESENTATION_REPRESENTATION('',(#98),#8779);
#55=TOROIDAL_SURFACE('',#5558,1.77525512860841,1.25);
#76=B_SPLINE_CURVE_WITH_KNOTS('',3,(#8451,#8452,#8453,#8454,#8455,#8456,
#8457,#8458,#8459,#8460),.UNSPECIFIED.,.F.,.F.,(4,2,2,2,4),(0.042485066523561,
0.0459790210316649,0.0922828710125633,0.139235462221755,0.187535404261205),
 .UNSPECIFIED.);
#77=B_SPLINE_CURVE_WITH_KNOTS('',3,(#8464,#8465,#8466,#8467,#8468,#8469,
#8470,#8471,#8472,#8473),.UNSPECIFIED.,.F.,.F.,(4,2,2,2,4),(0.589058059380764,
0.637358001420214,0.684310592629405,0.730614442610304,0.734108397118407),
 .UNSPECIFIED.);
#78=B_SPLINE_CURVE_WITH_KNOTS('',3,(#8485,#8486,#8487,#8488,#8489,#8490,
#8491,#8492,#8493,#8494),.UNSPECIFIED.,.F.,.F.,(4,2,2,2,4),(0.589058059380764,
0.637358001420214,0.684310592629405,0.730614442610304,0.734108397118408),
 .UNSPECIFIED.);
#79=B_SPLINE_CURVE_WITH_KNOTS('',3,(#8497,#8498,#8499,#8500,#8501,#8502,
#8503,#8504,#8505,#8506),.UNSPECIFIED.,.F.,.F.,(4,2,2,2,4),(0.0424850665235609,
0.0459790210316651,0.0922828710125635,0.139235462221755,0.187535404261205),
 .UNSPECIFIED.);
#84=SHAPE_REPRESENTATION_RELATIONSHIP('SRR','None',#8813,#91);
#91=ADVANCED_BREP_SHAPE_REPRESENTATION('',(#108),#8776);
#98=STYLED_ITEM('',(#8856),#108);
#108=MANIFOLD_SOLID_BREP('Body1',#5118);
#150=FACE_BOUND('',#994,.T.);
#303=CIRCLE('',#5548,3.);
#304=CIRCLE('',#5549,1.99137169252308);
#305=CIRCLE('',#5552,2.94442677252053);
#306=CIRCLE('',#5553,2.94442677252053);
#307=CIRCLE('',#5554,2.94442677252053);
#308=CIRCLE('',#5557,1.77525512860841);
#309=CIRCLE('',#5559,1.25);
#310=CIRCLE('',#5560,1.77525512860841);
#311=CIRCLE('',#5563,1.99137169252308);
#463=CYLINDRICAL_SURFACE('',#5564,1.99137169252308);
#680=FACE_OUTER_BOUND('',#993,.T.);
#681=FACE_OUTER_BOUND('',#995,.T.);
#682=FACE_OUTER_BOUND('',#996,.T.);
#683=FACE_OUTER_BOUND('',#997,.T.);
#684=FACE_OUTER_BOUND('',#998,.T.);
#685=FACE_OUTER_BOUND('',#999,.T.);
#686=FACE_OUTER_BOUND('',#1000,.T.);
#687=FACE_OUTER_BOUND('',#1001,.T.);
#688=FACE_OUTER_BOUND('',#1002,.T.);
#993=EDGE_LOOP('',(#4422));
#994=EDGE_LOOP('',(#4423));
#995=EDGE_LOOP('',(#4424,#4425,#4426,#4427));
#996=EDGE_LOOP('',(#4428,#4429,#4430,#4431,#4432));
#997=EDGE_LOOP('',(#4433,#4434,#4435,#4436));
#998=EDGE_LOOP('',(#4437,#4438));
#999=EDGE_LOOP('',(#4439,#4440,#4441,#4442,#4443,#4444,#4445,#4446,#4447,
#4448,#4449,#4450));
#1000=EDGE_LOOP('',(#4451,#4452));
#1001=EDGE_LOOP('',(#4453));
#1002=EDGE_LOOP('',(#4454,#4455,#4456,#4457));
#1541=LINE('',#8462,#2026);
#1542=LINE('',#8474,#2027);
#1543=LINE('',#8480,#2028);
#1544=LINE('',#8496,#2029);
#1545=LINE('',#8517,#2030);
#2026=VECTOR('',#6877,10.);
#2027=VECTOR('',#6878,10.);
#2028=VECTOR('',#6883,10.);
#2029=VECTOR('',#6890,10.);
#2030=VECTOR('',#6909,1.99137169252308);
#2448=VERTEX_POINT('',#8444);
#2449=VERTEX_POINT('',#8446);
#2450=VERTEX_POINT('',#8449);
#2451=VERTEX_POINT('',#8450);
#2452=VERTEX_POINT('',#8461);
#2453=VERTEX_POINT('',#8463);
#2454=VERTEX_POINT('',#8476);
#2455=VERTEX_POINT('',#8477);
#2456=VERTEX_POINT('',#8479);
#2457=VERTEX_POINT('',#8484);
#2458=VERTEX_POINT('',#8495);
#2459=VERTEX_POINT('',#8514);
#3115=EDGE_CURVE('',#2448,#2448,#303,.T.);
#3116=EDGE_CURVE('',#2449,#2449,#304,.T.);
#3117=EDGE_CURVE('',#2450,#2451,#76,.T.);
#3118=EDGE_CURVE('',#2452,#2450,#1541,.T.);
#3119=EDGE_CURVE('',#2453,#2452,#77,.T.);
#3120=EDGE_CURVE('',#2451,#2453,#1542,.T.);
#3121=EDGE_CURVE('',#2454,#2455,#305,.T.);
#3122=EDGE_CURVE('',#2454,#2456,#1543,.T.);
#3123=EDGE_CURVE('',#2452,#2456,#306,.T.);
#3124=EDGE_CURVE('',#2455,#2450,#307,.T.);
#3125=EDGE_CURVE('',#2457,#2454,#78,.T.);
#3126=EDGE_CURVE('',#2458,#2457,#1544,.T.);
#3127=EDGE_CURVE('',#2456,#2458,#79,.T.);
#3128=EDGE_CURVE('',#2451,#2453,#308,.T.);
#3129=EDGE_CURVE('',#2455,#2448,#309,.T.);
#3130=EDGE_CURVE('',#2458,#2457,#310,.T.);
#3131=EDGE_CURVE('',#2459,#2459,#311,.T.);
#3132=EDGE_CURVE('',#2449,#2459,#1545,.T.);
#4422=ORIENTED_EDGE('',*,*,#3115,.F.);
#4423=ORIENTED_EDGE('',*,*,#3116,.T.);
#4424=ORIENTED_EDGE('',*,*,#3117,.F.);
#4425=ORIENTED_EDGE('',*,*,#3118,.F.);
#4426=ORIENTED_EDGE('',*,*,#3119,.F.);
#4427=ORIENTED_EDGE('',*,*,#3120,.F.);
#4428=ORIENTED_EDGE('',*,*,#3121,.F.);
#4429=ORIENTED_EDGE('',*,*,#3122,.T.);
#4430=ORIENTED_EDGE('',*,*,#3123,.F.);
#4431=ORIENTED_EDGE('',*,*,#3118,.T.);
#4432=ORIENTED_EDGE('',*,*,#3124,.F.);
#4433=ORIENTED_EDGE('',*,*,#3125,.F.);
#4434=ORIENTED_EDGE('',*,*,#3126,.F.);
#4435=ORIENTED_EDGE('',*,*,#3127,.F.);
#4436=ORIENTED_EDGE('',*,*,#3122,.F.);
#4437=ORIENTED_EDGE('',*,*,#3120,.T.);
#4438=ORIENTED_EDGE('',*,*,#3128,.F.);
#4439=ORIENTED_EDGE('',*,*,#3121,.T.);
#4440=ORIENTED_EDGE('',*,*,#3129,.T.);
#4441=ORIENTED_EDGE('',*,*,#3115,.T.);
#4442=ORIENTED_EDGE('',*,*,#3129,.F.);
#4443=ORIENTED_EDGE('',*,*,#3124,.T.);
#4444=ORIENTED_EDGE('',*,*,#3117,.T.);
#4445=ORIENTED_EDGE('',*,*,#3128,.T.);
#4446=ORIENTED_EDGE('',*,*,#3119,.T.);
#4447=ORIENTED_EDGE('',*,*,#3123,.T.);
#4448=ORIENTED_EDGE('',*,*,#3127,.T.);
#4449=ORIENTED_EDGE('',*,*,#3130,.T.);
#4450=ORIENTED_EDGE('',*,*,#3125,.T.);
#4451=ORIENTED_EDGE('',*,*,#3126,.T.);
#4452=ORIENTED_EDGE('',*,*,#3130,.F.);
#4453=ORIENTED_EDGE('',*,*,#3131,.T.);
#4454=ORIENTED_EDGE('',*,*,#3116,.F.);
#4455=ORIENTED_EDGE('',*,*,#3132,.T.);
#4456=ORIENTED_EDGE('',*,*,#3131,.F.);
#4457=ORIENTED_EDGE('',*,*,#3132,.F.);
#4810=PLANE('',#5547);
#4811=PLANE('',#5550);
#4812=PLANE('',#5551);
#4813=PLANE('',#5555);
#4814=PLANE('',#5556);
#4815=PLANE('',#5561);
#4816=PLANE('',#5562);
#5042=ADVANCED_FACE('',(#680,#150),#4810,.F.);
#5043=ADVANCED_FACE('',(#681),#4811,.F.);
#5044=ADVANCED_FACE('',(#682),#4812,.F.);
#5045=ADVANCED_FACE('',(#683),#4813,.F.);
#5046=ADVANCED_FACE('',(#684),#4814,.T.);
#5047=ADVANCED_FACE('',(#685),#55,.T.);
#5048=ADVANCED_FACE('',(#686),#4815,.T.);
#5049=ADVANCED_FACE('',(#687),#4816,.F.);
#5050=ADVANCED_FACE('',(#688),#463,.T.);
#5118=CLOSED_SHELL('',(#5042,#5043,#5044,#5045,#5046,#5047,#5048,#5049,
#5050));
#5546=AXIS2_PLACEMENT_3D('',#8442,#6867,#6868);
#5547=AXIS2_PLACEMENT_3D('',#8443,#6869,#6870);
#5548=AXIS2_PLACEMENT_3D('',#8445,#6871,#6872);
#5549=AXIS2_PLACEMENT_3D('',#8447,#6873,#6874);
#5550=AXIS2_PLACEMENT_3D('',#8448,#6875,#6876);
#5551=AXIS2_PLACEMENT_3D('',#8475,#6879,#6880);
#5552=AXIS2_PLACEMENT_3D('',#8478,#6881,#6882);
#5553=AXIS2_PLACEMENT_3D('',#8481,#6884,#6885);
#5554=AXIS2_PLACEMENT_3D('',#8482,#6886,#6887);
#5555=AXIS2_PLACEMENT_3D('',#8483,#6888,#6889);
#5556=AXIS2_PLACEMENT_3D('',#8507,#6891,#6892);
#5557=AXIS2_PLACEMENT_3D('',#8508,#6893,#6894);
#5558=AXIS2_PLACEMENT_3D('',#8509,#6895,#6896);
#5559=AXIS2_PLACEMENT_3D('',#8510,#6897,#6898);
#5560=AXIS2_PLACEMENT_3D('',#8511,#6899,#6900);
#5561=AXIS2_PLACEMENT_3D('',#8512,#6901,#6902);
#5562=AXIS2_PLACEMENT_3D('',#8513,#6903,#6904);
#5563=AXIS2_PLACEMENT_3D('',#8515,#6905,#6906);
#5564=AXIS2_PLACEMENT_3D('',#8516,#6907,#6908);
#6867=DIRECTION('axis',(0.,0.,1.));
#6868=DIRECTION('refdir',(1.,0.,0.));
#6869=DIRECTION('center_axis',(0.,-1.,0.));
#6870=DIRECTION('ref_axis',(1.,0.,0.));
#6871=DIRECTION('center_axis',(0.,-1.,0.));
#6872=DIRECTION('ref_axis',(1.,0.,0.));
#6873=DIRECTION('center_axis',(0.,-1.,0.));
#6874=DIRECTION('ref_axis',(1.,0.,0.));
#6875=DIRECTION('center_axis',(0.,0.,-1.));
#6876=DIRECTION('ref_axis',(0.,1.,0.));
#6877=DIRECTION('',(1.,0.,0.));
#6878=DIRECTION('',(-1.,0.,0.));
#6879=DIRECTION('center_axis',(0.,1.,0.));
#6880=DIRECTION('ref_axis',(0.,0.,1.));
#6881=DIRECTION('center_axis',(0.,1.,0.));
#6882=DIRECTION('ref_axis',(0.,0.,-1.));
#6883=DIRECTION('',(-1.,0.,0.));
#6884=DIRECTION('center_axis',(0.,1.,0.));
#6885=DIRECTION('ref_axis',(0.,0.,-1.));
#6886=DIRECTION('center_axis',(0.,1.,0.));
#6887=DIRECTION('ref_axis',(0.,0.,-1.));
#6888=DIRECTION('center_axis',(0.,0.,1.));
#6889=DIRECTION('ref_axis',(0.,-1.,0.));
#6890=DIRECTION('',(1.,0.,0.));
#6891=DIRECTION('center_axis',(0.,-1.,0.));
#6892=DIRECTION('ref_axis',(1.,0.,0.));
#6893=DIRECTION('center_axis',(0.,1.,0.));
#6894=DIRECTION('ref_axis',(-1.,0.,0.));
#6895=DIRECTION('center_axis',(0.,-1.,0.));
#6896=DIRECTION('ref_axis',(-1.,0.,0.));
#6897=DIRECTION('center_axis',(0.,0.,1.));
#6898=DIRECTION('ref_axis',(1.,0.,0.));
#6899=DIRECTION('center_axis',(0.,1.,0.));
#6900=DIRECTION('ref_axis',(-1.,0.,0.));
#6901=DIRECTION('center_axis',(0.,-1.,0.));
#6902=DIRECTION('ref_axis',(1.,0.,0.));
#6903=DIRECTION('center_axis',(0.,-1.,0.));
#6904=DIRECTION('ref_axis',(1.,0.,0.));
#6905=DIRECTION('center_axis',(0.,1.,0.));
#6906=DIRECTION('ref_axis',(1.,0.,0.));
#6907=DIRECTION('center_axis',(0.,-1.,0.));
#6908=DIRECTION('ref_axis',(1.,0.,0.));
#6909=DIRECTION('',(0.,1.,0.));
#8442=CARTESIAN_POINT('',(0.,0.,0.));
#8443=CARTESIAN_POINT('Origin',(0.,-6.5,48.6364583401654));
#8444=CARTESIAN_POINT('',(3.,-6.5,48.6364583401654));
#8445=CARTESIAN_POINT('Origin',(0.,-6.5,48.6364583401654));
#8446=CARTESIAN_POINT('',(-1.99137169252308,-6.5,48.6364583401654));
#8447=CARTESIAN_POINT('Origin',(0.,-6.5,48.6364583401654));
#8448=CARTESIAN_POINT('Origin',(0.,-8.30780358767644,48.1364583401654));
#8449=CARTESIAN_POINT('',(2.90166314701339,-6.69219641232357,48.1364583401654));
#8450=CARTESIAN_POINT('',(1.70338802732979,-7.5,48.1364583401654));
#8451=CARTESIAN_POINT('Ctrl Pts',(2.90166314701339,-6.69219641232357,48.1364583401654));
#8452=CARTESIAN_POINT('Ctrl Pts',(2.89738588729895,-6.70334128000014,48.1364583401654));
#8453=CARTESIAN_POINT('Ctrl Pts',(2.89299471233252,-6.7143000212193,48.1364583401654));
#8454=CARTESIAN_POINT('Ctrl Pts',(2.8291108799372,-6.86750715654011,48.1364583401654));
#8455=CARTESIAN_POINT('Ctrl Pts',(2.72552921913,-7.02105058333943,48.1364583401654));
#8456=CARTESIAN_POINT('Ctrl Pts',(2.50478431602599,-7.23991674541786,48.1364583401654));
#8457=CARTESIAN_POINT('Ctrl Pts',(2.34795167915788,-7.34324272062795,48.1364583401654));
#8458=CARTESIAN_POINT('Ctrl Pts',(2.05411736736806,-7.46354654155341,48.1364583401654));
#8459=CARTESIAN_POINT('Ctrl Pts',(1.86438783412795,-7.5,48.1364583401654));
#8460=CARTESIAN_POINT('Ctrl Pts',(1.70338802732979,-7.5,48.1364583401654));
#8461=CARTESIAN_POINT('',(-2.90166314701339,-6.69219641232357,48.1364583401654));
#8462=CARTESIAN_POINT('',(0.,-6.69219641232357,48.1364583401654));
#8463=CARTESIAN_POINT('',(-1.70338802732979,-7.5,48.1364583401654));
#8464=CARTESIAN_POINT('Ctrl Pts',(-1.70338802732979,-7.5,48.1364583401654));
#8465=CARTESIAN_POINT('Ctrl Pts',(-1.86438783412795,-7.5,48.1364583401654));
#8466=CARTESIAN_POINT('Ctrl Pts',(-2.05411736736806,-7.46354654155341,48.1364583401654));
#8467=CARTESIAN_POINT('Ctrl Pts',(-2.34795167915788,-7.34324272062795,48.1364583401654));
#8468=CARTESIAN_POINT('Ctrl Pts',(-2.50478431602599,-7.23991674541786,48.1364583401654));
#8469=CARTESIAN_POINT('Ctrl Pts',(-2.72552921913,-7.02105058333943,48.1364583401654));
#8470=CARTESIAN_POINT('Ctrl Pts',(-2.8291108799372,-6.86750715654011,48.1364583401654));
#8471=CARTESIAN_POINT('Ctrl Pts',(-2.89299471233252,-6.7143000212193,48.1364583401654));
#8472=CARTESIAN_POINT('Ctrl Pts',(-2.89738588729895,-6.70334128000014,48.1364583401654));
#8473=CARTESIAN_POINT('Ctrl Pts',(-2.90166314701339,-6.69219641232357,48.1364583401654));
#8474=CARTESIAN_POINT('',(0.,-7.5,48.1364583401654));
#8475=CARTESIAN_POINT('Origin',(0.,-6.69219641232357,48.1364583401654));
#8476=CARTESIAN_POINT('',(2.90166314701339,-6.69219641232357,49.1364583401654));
#8477=CARTESIAN_POINT('',(2.94442677252053,-6.69219641232357,48.6364583401654));
#8478=CARTESIAN_POINT('Origin',(0.,-6.69219641232357,48.6364583401654));
#8479=CARTESIAN_POINT('',(-2.90166314701339,-6.69219641232357,49.1364583401654));
#8480=CARTESIAN_POINT('',(0.,-6.69219641232357,49.1364583401654));
#8481=CARTESIAN_POINT('Origin',(0.,-6.69219641232357,48.6364583401654));
#8482=CARTESIAN_POINT('Origin',(0.,-6.69219641232357,48.6364583401654));
#8483=CARTESIAN_POINT('Origin',(0.,-6.69219641232357,49.1364583401654));
#8484=CARTESIAN_POINT('',(1.70338802732979,-7.5,49.1364583401654));
#8485=CARTESIAN_POINT('Ctrl Pts',(1.70338802732979,-7.5,49.1364583401654));
#8486=CARTESIAN_POINT('Ctrl Pts',(1.86438783412795,-7.5,49.1364583401654));
#8487=CARTESIAN_POINT('Ctrl Pts',(2.05411736736806,-7.46354654155341,49.1364583401654));
#8488=CARTESIAN_POINT('Ctrl Pts',(2.34795167915788,-7.34324272062795,49.1364583401654));
#8489=CARTESIAN_POINT('Ctrl Pts',(2.50478431602599,-7.23991674541786,49.1364583401654));
#8490=CARTESIAN_POINT('Ctrl Pts',(2.72552921913,-7.02105058333943,49.1364583401654));
#8491=CARTESIAN_POINT('Ctrl Pts',(2.8291108799372,-6.86750715654011,49.1364583401654));
#8492=CARTESIAN_POINT('Ctrl Pts',(2.89299471233252,-6.7143000212193,49.1364583401654));
#8493=CARTESIAN_POINT('Ctrl Pts',(2.89738588729895,-6.70334128000014,49.1364583401654));
#8494=CARTESIAN_POINT('Ctrl Pts',(2.90166314701339,-6.69219641232357,49.1364583401654));
#8495=CARTESIAN_POINT('',(-1.70338802732979,-7.5,49.1364583401654));
#8496=CARTESIAN_POINT('',(0.,-7.5,49.1364583401654));
#8497=CARTESIAN_POINT('Ctrl Pts',(-2.90166314701339,-6.69219641232357,49.1364583401654));
#8498=CARTESIAN_POINT('Ctrl Pts',(-2.89738588729895,-6.70334128000014,49.1364583401654));
#8499=CARTESIAN_POINT('Ctrl Pts',(-2.89299471233252,-6.7143000212193,49.1364583401654));
#8500=CARTESIAN_POINT('Ctrl Pts',(-2.8291108799372,-6.86750715654011,49.1364583401654));
#8501=CARTESIAN_POINT('Ctrl Pts',(-2.72552921913,-7.02105058333943,49.1364583401654));
#8502=CARTESIAN_POINT('Ctrl Pts',(-2.50478431602599,-7.23991674541786,49.1364583401654));
#8503=CARTESIAN_POINT('Ctrl Pts',(-2.34795167915788,-7.34324272062795,49.1364583401654));
#8504=CARTESIAN_POINT('Ctrl Pts',(-2.05411736736806,-7.46354654155341,49.1364583401654));
#8505=CARTESIAN_POINT('Ctrl Pts',(-1.86438783412795,-7.5,49.1364583401654));
#8506=CARTESIAN_POINT('Ctrl Pts',(-1.70338802732979,-7.5,49.1364583401654));
#8507=CARTESIAN_POINT('Origin',(0.,-7.5,48.6364583401654));
#8508=CARTESIAN_POINT('Origin',(0.,-7.5,48.6364583401654));
#8509=CARTESIAN_POINT('Origin',(0.,-6.25,48.6364583401654));
#8510=CARTESIAN_POINT('Origin',(1.77525512860841,-6.25,48.6364583401654));
#8511=CARTESIAN_POINT('Origin',(0.,-7.5,48.6364583401654));
#8512=CARTESIAN_POINT('Origin',(0.,-7.5,48.6364583401654));
#8513=CARTESIAN_POINT('Origin',(0.,-2.5,48.6364583401654));
#8514=CARTESIAN_POINT('',(-1.99137169252308,-2.5,48.6364583401654));
#8515=CARTESIAN_POINT('Origin',(0.,-2.5,48.6364583401654));
#8516=CARTESIAN_POINT('Origin',(0.,-6.,48.6364583401654));
#8517=CARTESIAN_POINT('',(-1.99137169252308,-6.,48.6364583401654));
#8767=UNCERTAINTY_MEASURE_WITH_UNIT(LENGTH_MEASURE(0.01),#8780,
'DISTANCE_ACCURACY_VALUE',
'Maximum model space distance between geometric entities at asserted c
onnectivities');
#8770=UNCERTAINTY_MEASURE_WITH_UNIT(LENGTH_MEASURE(0.01),#8780,
'DISTANCE_ACCURACY_VALUE',
'Maximum model space distance between geometric entities at asserted c
onnectivities');
#8776=(
GEOMETRIC_REPRESENTATION_CONTEXT(3)
GLOBAL_UNCERTAINTY_ASSIGNED_CONTEXT((#8767))
GLOBAL_UNIT_ASSIGNED_CONTEXT((#8780,#8782,#8783))
REPRESENTATION_CONTEXT('','3D')
);
#8779=(
GEOMETRIC_REPRESENTATION_CONTEXT(3)
GLOBAL_UNCERTAINTY_ASSIGNED_CONTEXT((#8770))
GLOBAL_UNIT_ASSIGNED_CONTEXT((#8780,#8782,#8783))
REPRESENTATION_CONTEXT('','3D')
);
#8780=(
LENGTH_UNIT()
NAMED_UNIT(*)
SI_UNIT(.MILLI.,.METRE.)
);
#8782=(
NAMED_UNIT(*)
PLANE_ANGLE_UNIT()
SI_UNIT($,.RADIAN.)
);
#8783=(
NAMED_UNIT(*)
SI_UNIT($,.STERADIAN.)
SOLID_ANGLE_UNIT()
);
#8789=SHAPE_DEFINITION_REPRESENTATION(#8797,#8813);
#8797=PRODUCT_DEFINITION_SHAPE('',$,#8822);
#8813=SHAPE_REPRESENTATION('',(#5546),#8776);
#8816=PRODUCT_DEFINITION_CONTEXT('part definition',#8842,'design');
#8822=PRODUCT_DEFINITION('Screw','Screw',#8830,#8816);
#8830=PRODUCT_DEFINITION_FORMATION('',$,#8849);
#8842=APPLICATION_CONTEXT(
'Core Data for Automotive Mechanical Design Process');
#8843=PRODUCT_CONTEXT('part definition',#8842,'mechanical');
#8849=PRODUCT('Screw','Screw',$,(#8843));
#8856=PRESENTATION_STYLE_ASSIGNMENT((#8861));
#8861=SURFACE_STYLE_USAGE(.BOTH.,#8866);
#8866=SURFACE_SIDE_STYLE('',(#8871));
#8871=SURFACE_STYLE_FILL_AREA(#8876);
#8876=FILL_AREA_STYLE('Opaque(160,160,160)',(#8881));
#8881=FILL_AREA_STYLE_COLOUR('Opaque(160,160,160)',#8886);
#8886=COLOUR_RGB('Opaque(160,160,160)', 0.72549020, 0.75294118, 0.79215686);
ENDSEC;
END-ISO-10303-21;
